ISO-10303-21;
HEADER;
FILE_DESCRIPTION (('STEP AP214'),
    '1' );
FILE_NAME ('socket head cap screw_iso_ISO 4762 M5 x 8 - 8N.step',
    '2026-10-08T14:41:38',
    ( '' ),
    ( '' ),
    'SwSTEP 2.0',
    'SolidWorks 2026',
    '' );
FILE_SCHEMA (( 'AUTOMOTIVE_DESIGN' ));
ENDSEC;

DATA;
#33=DIRECTION ( 'NONE',  ( 0.000000000000000000, 0.4999999999999991118, -0.8660254037844391517 ) ) ;
#40=CARTESIAN_POINT ( 'NONE',  ( 2.500000000000000000, 0.000000000000000000, 0.000000000000000000 ) ) ;
#66=CYLINDRICAL_SURFACE ( 'NONE', #13079, 2.500000000000000444 ) ;
#71=DIRECTION ( 'NONE',  ( -1.000000000000000000, -0.000000000000000000, -0.000000000000000000 ) ) ;
#91=DIRECTION ( 'NONE',  ( 0.000000000000000000, -0.4999999999999993894, 0.8660254037844389297 ) ) ;
#111=VERTEX_POINT ( 'NONE', #2135 ) ;
#219=DIRECTION ( 'NONE',  ( -1.000000000000000000, -0.000000000000000000, -0.000000000000000000 ) ) ;
#242=EDGE_LOOP ( 'NONE', ( #10443, #19008, #2745 ) ) ;
#329=SURFACE_STYLE_USAGE ( .BOTH. , #10800 ) ;
#340=DIRECTION ( 'NONE',  ( 1.000000000000000000, 0.000000000000000000, 0.000000000000000000 ) ) ;
#377=EDGE_CURVE ( 'NONE', #14750, #2431, #8581, .T. ) ;
#383=DIRECTION ( 'NONE',  ( -1.000000000000000000, -0.000000000000000000, -0.000000000000000000 ) ) ;
#401=ORIENTED_EDGE ( 'NONE', *, *, #9823, .T. ) ;
#411=PLANE ( 'NONE',  #5533 ) ;
#426=EDGE_LOOP ( 'NONE', ( #14874, #12807, #12078, #5130, #11922 ) ) ;
#427=CARTESIAN_POINT ( 'NONE',  ( 0.2500000000000002220, 4.898587196589412829E-16, -4.000000000000000000 ) ) ;
#469=ORIENTED_EDGE ( 'NONE', *, *, #9014, .T. ) ;
#513=VERTEX_POINT ( 'NONE', #10239 ) ;
#524=CARTESIAN_POINT ( 'NONE',  ( 2.500000000000000000, 2.357898499370431722, -2.818925648462311528E-15 ) ) ;
#610=FILL_AREA_STYLE ('',( #3268 ) ) ;
#615=DIRECTION ( 'NONE',  ( 0.000000000000000000, 0.000000000000000000, 1.000000000000000000 ) ) ;
#632=EDGE_CURVE ( 'NONE', #7648, #3232, #16629, .T. ) ;
#641=EDGE_CURVE ( 'NONE', #12504, #12460, #12102, .T. ) ;
#702=FACE_OUTER_BOUND ( 'NONE', #9718, .T. ) ;
#712=LINE ( 'NONE', #8437, #14065 ) ;
#721=CARTESIAN_POINT ( 'NONE',  ( 2.500000000000000000, 3.004629197474319246E-15, 2.042000000000000259 ) ) ;
#770=COLOUR_RGB ( '', 0.09019608, 0.27058824, 0.51372549) ;
#800=CARTESIAN_POINT ( 'NONE',  ( 0.000000000000000000, 1.178949249685212974, -2.042000000000001148 ) ) ;
#815=AXIS2_PLACEMENT_3D ( 'NONE', #12603, #5162, #11125 ) ;
#820=DIRECTION ( 'NONE',  ( 0.000000000000000000, 0.000000000000000000, 1.000000000000000000 ) ) ;
#828=CIRCLE ( 'NONE', #10842, 2.500000000000000444 ) ;
#846=DIRECTION ( 'NONE',  ( 0.000000000000000000, 0.000000000000000000, 1.000000000000000000 ) ) ;
#877=CARTESIAN_POINT ( 'NONE',  ( 0.000000000000000000, 0.000000000000000000, 0.000000000000000000 ) ) ;
#892=DIRECTION ( 'NONE',  ( 0.000000000000000000, 0.8660254037844380415, -0.5000000000000012212 ) ) ;
#939=CARTESIAN_POINT ( 'NONE',  ( 2.500000000000000000, -1.178949249685214307, 2.042000000000002036 ) ) ;
#954=ORIENTED_EDGE ( 'NONE', *, *, #9245, .F. ) ;
#984=CIRCLE ( 'NONE', #14440, 2.041999999999999815 ) ;
#992=PLANE ( 'NONE',  #18189 ) ;
#996=VERTEX_POINT ( 'NONE', #17478 ) ;
#1014=FACE_OUTER_BOUND ( 'NONE', #6410, .T. ) ;
#1037=DIRECTION ( 'NONE',  ( -0.000000000000000000, 1.471414886128461471E-15, 1.000000000000000000 ) ) ;
#1063=DIRECTION ( 'NONE',  ( -1.000000000000000000, -0.000000000000000000, -0.000000000000000000 ) ) ;
#1071=ORIENTED_EDGE ( 'NONE', *, *, #17380, .T. ) ;
#1076=ORIENTED_EDGE ( 'NONE', *, *, #9823, .F. ) ;
#1083=ORIENTED_EDGE ( 'NONE', *, *, #3878, .T. ) ;
#1101=CONICAL_SURFACE ( 'NONE', #9558, 2.055000000000000160, 0.7853981633974712606 ) ;
#1137=CARTESIAN_POINT ( 'NONE',  ( -31.74999999999995737, 5.204748896376250699E-16, -4.250000000000000000 ) ) ;
#1166=DIRECTION ( 'NONE',  ( 0.000000000000000000, 0.000000000000000000, 1.000000000000000000 ) ) ;
#1262=DIRECTION ( 'NONE',  ( -1.000000000000000000, -0.000000000000000000, -0.000000000000000000 ) ) ;
#1265=AXIS2_PLACEMENT_3D ( 'NONE', #12829, #9974, #15788 ) ;
#1289=PRODUCT_DEFINITION_SHAPE ( 'NONE', 'NONE',  #18072 ) ;
#1382=CARTESIAN_POINT ( 'NONE',  ( 12.99999999999999822, 0.000000000000000000, 0.000000000000000000 ) ) ;
#1391=CYLINDRICAL_SURFACE ( 'NONE', #7577, 2.500000000000000444 ) ;
#1443=TOROIDAL_SURFACE ( 'NONE', #2378, 2.700000000000000622, 0.2000000000000000111 ) ;
#1449=PRODUCT ( 'socket head cap screw_iso_ISO 4762 M5 x 8 - 8N', 'socket head cap screw_iso_ISO 4762 M5 x 8 - 8N', '', ( #10192 ) ) ;
#1457=EDGE_CURVE ( 'NONE', #4615, #996, #11236, .T. ) ;
#1480=CIRCLE ( 'NONE', #3362, 4.000000000000000000 ) ;
#1522=AXIS2_PLACEMENT_3D ( 'NONE', #18304, #18691, #9555 ) ;
#1523=FILL_AREA_STYLE_COLOUR ( '', #770 ) ;
#1563=VECTOR ( 'NONE', #33, 1000.000000000000000 ) ;
#1635=FACE_OUTER_BOUND ( 'NONE', #15494, .T. ) ;
#1712=STYLED_ITEM ( 'NONE', ( #13172 ), #16479 ) ;
#1736=VERTEX_POINT ( 'NONE', #11943 ) ;
#1738=EDGE_CURVE ( 'NONE', #5670, #2431, #7535, .T. ) ;
#1745=TOROIDAL_SURFACE ( 'NONE', #5211, 4.000000000000000000, 0.2500000000000000000 ) ;
#1778=VECTOR ( 'NONE', #16337, 1000.000000000000114 ) ;
#1791=AXIS2_PLACEMENT_3D ( 'NONE', #13713, #4815, #7646 ) ;
#1818=DIRECTION ( 'NONE',  ( 0.000000000000000000, 0.4999999999999993894, -0.8660254037844389297 ) ) ;
#1871=CONICAL_SURFACE ( 'NONE', #2791, 2.041999999999999815, 1.047197551196591858 ) ;
#1885=FACE_OUTER_BOUND ( 'NONE', #13424, .T. ) ;
#1889=CARTESIAN_POINT ( 'NONE',  ( 3.678949249685231848, 1.601138781673192758E-19, 0.000000000000000000 ) ) ;
#1898=CARTESIAN_POINT ( 'NONE',  ( 4.999999999999997335, 0.000000000000000000, 4.250000000000000000 ) ) ;
#1955=DIRECTION ( 'NONE',  ( -1.000000000000000000, -0.000000000000000000, -0.000000000000000000 ) ) ;
#1964=EDGE_CURVE ( 'NONE', #9967, #3035, #9767, .T. ) ;
#1984=DIRECTION ( 'NONE',  ( -0.000000000000000000, 0.8660254037844391517, 0.4999999999999991673 ) ) ;
#1985=EDGE_LOOP ( 'NONE', ( #1083, #16673, #18572, #9771 ) ) ;
#1994=CARTESIAN_POINT ( 'NONE',  ( 5.199999999999996625, 0.000000000000000000, 0.000000000000000000 ) ) ;
#2044=CARTESIAN_POINT ( 'NONE',  ( 0.2500000000000002220, 0.000000000000000000, 0.000000000000000000 ) ) ;
#2068=APPLICATION_CONTEXT ( 'automotive_design' ) ;
#2099=EDGE_CURVE ( 'NONE', #17064, #8108, #14045, .T. ) ;
#2101=EDGE_CURVE ( 'NONE', #16545, #10270, #8584, .T. ) ;
#2135=CARTESIAN_POINT ( 'NONE',  ( 2.500000000000000000, -1.178949249685218970, -2.041999999999998039 ) ) ;
#2206=AXIS2_PLACEMENT_3D ( 'NONE', #3640, #15597, #5215 ) ;
#2213=CARTESIAN_POINT ( 'NONE',  ( 4.999999999999997335, 5.204748896376250699E-16, -4.250000000000000000 ) ) ;
#2215=LINE ( 'NONE', #3970, #7707 ) ;
#2225=VECTOR ( 'NONE', #9876, 1000.000000000000114 ) ;
#2238=DIRECTION ( 'NONE',  ( 0.000000000000000000, 0.000000000000000000, -1.000000000000000000 ) ) ;
#2249=VECTOR ( 'NONE', #7326, 1000.000000000000000 ) ;
#2309=ADVANCED_FACE ( 'NONE', ( #8875 ), #66, .T. ) ;
#2338=MECHANICAL_DESIGN_GEOMETRIC_PRESENTATION_REPRESENTATION('',(#1712),#10473);
#2347=ORIENTED_EDGE ( 'NONE', *, *, #1457, .T. ) ;
#2378=AXIS2_PLACEMENT_3D ( 'NONE', #6617, #3761, #18579 ) ;
#2388=CARTESIAN_POINT ( 'NONE',  ( 2.500000000000000000, 1.768423874527822459, -1.021000000000002794 ) ) ;
#2408=CARTESIAN_POINT ( 'NONE',  ( 2.500000000000000000, 2.357898499370431722, -2.818925648462311528E-15 ) ) ;
#2431=VERTEX_POINT ( 'NONE', #14070 ) ;
#2433=EDGE_CURVE ( 'NONE', #13613, #16356, #9943, .T. ) ;
#2441=CARTESIAN_POINT ( 'NONE',  ( 13.00000000000000000, 2.055000000000000160, 0.000000000000000000 ) ) ;
#2451=DIRECTION ( 'NONE',  ( -1.000000000000000000, -0.000000000000000000, -0.000000000000000000 ) ) ;
#2514=ORIENTED_EDGE ( 'NONE', *, *, #632, .F. ) ;
#2518=ORIENTED_EDGE ( 'NONE', *, *, #2101, .T. ) ;
#2555=CARTESIAN_POINT ( 'NONE',  ( 2.500000000000000000, 2.357898499370431722, -2.818925648462311528E-15 ) ) ;
#2591=FILL_AREA_STYLE ('',( #1523 ) ) ;
#2627=FACE_OUTER_BOUND ( 'NONE', #3409, .T. ) ;
#2653=CARTESIAN_POINT ( 'NONE',  ( 12.99999999999999822, 2.789133085058097101E-16, -2.055000000000000160 ) ) ;
#2660=CARTESIAN_POINT ( 'NONE',  ( 5.199999999999996625, 0.000000000000000000, 0.000000000000000000 ) ) ;
#2667=VECTOR ( 'NONE', #16932, 1000.000000000000000 ) ;
#2709=LINE ( 'NONE', #10442, #9883 ) ;
#2745=ORIENTED_EDGE ( 'NONE', *, *, #2099, .F. ) ;
#2791=AXIS2_PLACEMENT_3D ( 'NONE', #16606, #9441, #615 ) ;
#2795=AXIS2_PLACEMENT_3D ( 'NONE', #1994, #15521, #13948 ) ;
#2830=( GEOMETRIC_REPRESENTATION_CONTEXT ( 3 ) GLOBAL_UNCERTAINTY_ASSIGNED_CONTEXT ( ( #12586 ) ) GLOBAL_UNIT_ASSIGNED_CONTEXT ( ( #3654, #9623, #17088 ) ) REPRESENTATION_CONTEXT ( 'NONE', 'WORKASPACE' ) );
#2851=ORIENTED_EDGE ( 'NONE', *, *, #4080, .T. ) ;
#2870=CARTESIAN_POINT ( 'NONE',  ( 4.999999999999999112, 0.000000000000000000, 0.000000000000000000 ) ) ;
#2920=ORIENTED_EDGE ( 'NONE', *, *, #11885, .T. ) ;
#2977=CARTESIAN_POINT ( 'NONE',  ( 12.55500000000001748, 0.000000000000000000, 0.000000000000000000 ) ) ;
#2979=VECTOR ( 'NONE', #6699, 999.9999999999997726 ) ;
#3035=VERTEX_POINT ( 'NONE', #14114 ) ;
#3119=ORIENTED_EDGE ( 'NONE', *, *, #4240, .F. ) ;
#3125=VECTOR ( 'NONE', #14120, 1000.000000000000000 ) ;
#3232=VERTEX_POINT ( 'NONE', #8695 ) ;
#3260=ADVANCED_FACE ( 'NONE', ( #1014 ), #6880, .T. ) ;
#3268=FILL_AREA_STYLE_COLOUR ( '', #17539 ) ;
#3333=ORIENTED_EDGE ( 'NONE', *, *, #12131, .F. ) ;
#3356=LINE ( 'NONE', #9321, #16496 ) ;
#3359=PLANE ( 'NONE',  #14258 ) ;
#3360=ORIENTED_EDGE ( 'NONE', *, *, #377, .F. ) ;
#3362=AXIS2_PLACEMENT_3D ( 'NONE', #9801, #14504, #15795 ) ;
#3371=LINE ( 'NONE', #524, #2979 ) ;
#3409=EDGE_LOOP ( 'NONE', ( #14733, #16648 ) ) ;
#3447=EDGE_CURVE ( 'NONE', #16356, #12614, #13465, .T. ) ;
#3472=AXIS2_PLACEMENT_3D ( 'NONE', #3916, #5581, #12924 ) ;
#3546=EDGE_CURVE ( 'NONE', #17266, #513, #18175, .T. ) ;
#3550=DIRECTION ( 'NONE',  ( -0.5000000000000051070, 0.000000000000000000, 0.8660254037844355990 ) ) ;
#3556=ADVANCED_FACE ( 'NONE', ( #8743 ), #14732, .T. ) ;
#3565=CARTESIAN_POINT ( 'NONE',  ( 4.999999999999999112, 4.250000000000000000, 0.000000000000000000 ) ) ;
#3611=MANIFOLD_SOLID_BREP ( 'Hex', #17932 ) ;
#3612=CARTESIAN_POINT ( 'NONE',  ( 0.2500000000000002220, 0.000000000000000000, 4.000000000000000000 ) ) ;
#3619=VERTEX_POINT ( 'NONE', #1898 ) ;
#3640=CARTESIAN_POINT ( 'NONE',  ( 2.500000000000000000, 0.000000000000000000, 0.000000000000000000 ) ) ;
#3654=( LENGTH_UNIT ( ) NAMED_UNIT ( * ) SI_UNIT ( .MILLI., .METRE. ) );
#3664=EDGE_CURVE ( 'NONE', #3619, #15191, #12661, .T. ) ;
#3673=FACE_OUTER_BOUND ( 'NONE', #17092, .T. ) ;
#3690=APPLICATION_CONTEXT ( 'automotive_design' ) ;
#3696=CARTESIAN_POINT ( 'NONE',  ( 2.500000000000000000, -1.768423874527825124, -1.020999999999998575 ) ) ;
#3701=ADVANCED_FACE ( 'NONE', ( #6788 ), #992, .F. ) ;
#3722=VERTEX_POINT ( 'NONE', #800 ) ;
#3761=DIRECTION ( 'NONE',  ( 1.000000000000000000, 0.000000000000000000, 0.000000000000000000 ) ) ;
#3768=AXIS2_PLACEMENT_3D ( 'NONE', #19053, #10214, #5727 ) ;
#3795=EDGE_CURVE ( 'NONE', #16140, #996, #19224, .T. ) ;
#3878=EDGE_CURVE ( 'NONE', #12574, #7648, #9420, .T. ) ;
#3904=CARTESIAN_POINT ( 'NONE',  ( 2.500000000000000000, 1.178949249685212974, -2.042000000000001148 ) ) ;
#3916=CARTESIAN_POINT ( 'NONE',  ( -31.74999999999995737, 0.000000000000000000, 0.000000000000000000 ) ) ;
#3947=CIRCLE ( 'NONE', #19285, 0.2500000000000002220 ) ;
#3970=CARTESIAN_POINT ( 'NONE',  ( 2.500000000000000000, 2.357898499370431722, -2.818925648462311528E-15 ) ) ;
#4060=CIRCLE ( 'NONE', #19074, 2.041999999999999815 ) ;
#4063=DIRECTION ( 'NONE',  ( 0.000000000000000000, -0.4999999999999993894, 0.8660254037844389297 ) ) ;
#4080=EDGE_CURVE ( 'NONE', #996, #12504, #7758, .T. ) ;
#4103=ORIENTED_EDGE ( 'NONE', *, *, #12131, .T. ) ;
#4191=ORIENTED_EDGE ( 'NONE', *, *, #3664, .T. ) ;
#4208=EDGE_CURVE ( 'NONE', #513, #111, #15778, .T. ) ;
#4212=DIRECTION ( 'NONE',  ( 0.000000000000000000, 0.5000000000000011102, 0.8660254037844380415 ) ) ;
#4222=EDGE_CURVE ( 'NONE', #14750, #12460, #9962, .T. ) ;
#4240=EDGE_CURVE ( 'NONE', #6956, #2431, #7037, .T. ) ;
#4355=CARTESIAN_POINT ( 'NONE',  ( 0.000000000000000000, -1.178949249685218970, -2.041999999999998039 ) ) ;
#4401=ORIENTED_EDGE ( 'NONE', *, *, #18393, .F. ) ;
#4438=AXIS2_PLACEMENT_3D ( 'NONE', #18478, #5046, #11008 ) ;
#4489=EDGE_LOOP ( 'NONE', ( #469, #9331, #4934, #16736, #15181 ) ) ;
#4502=CARTESIAN_POINT ( 'NONE',  ( 2.500000000000000000, 1.178949249685217193, 2.041999999999998483 ) ) ;
#4578=DIRECTION ( 'NONE',  ( -1.000000000000000000, -0.000000000000000000, -0.000000000000000000 ) ) ;
#4591=ORIENTED_EDGE ( 'NONE', *, *, #3546, .F. ) ;
#4602=ADVANCED_FACE ( 'NONE', ( #14466 ), #15757, .F. ) ;
#4615=VERTEX_POINT ( 'NONE', #3696 ) ;
#4652=CARTESIAN_POINT ( 'NONE',  ( 2.500000000000000000, 2.357898499370431722, -2.818925648462311528E-15 ) ) ;
#4707=CARTESIAN_POINT ( 'NONE',  ( 2.500000000000000000, 0.000000000000000000, 0.000000000000000000 ) ) ;
#4727=VERTEX_POINT ( 'NONE', #2408 ) ;
#4734=STYLED_ITEM ( 'NONE', ( #6506 ), #3611 ) ;
#4753=CARTESIAN_POINT ( 'NONE',  ( 2.500000000000000000, 2.500728763858895382E-16, -2.041999999999999815 ) ) ;
#4815=DIRECTION ( 'NONE',  ( 0.000000000000000000, 0.000000000000000000, 1.000000000000000000 ) ) ;
#4877=CARTESIAN_POINT ( 'NONE',  ( 2.500000000000000000, -2.357898499370432610, 3.252606517456513302E-15 ) ) ;
#4887=VECTOR ( 'NONE', #3550, 1000.000000000000114 ) ;
#4893=ORIENTED_EDGE ( 'NONE', *, *, #2433, .T. ) ;
#4900=EDGE_CURVE ( 'NONE', #3619, #16545, #13141, .T. ) ;
#4910=ORIENTED_EDGE ( 'NONE', *, *, #15426, .T. ) ;
#4934=ORIENTED_EDGE ( 'NONE', *, *, #4208, .F. ) ;
#4939=UNCERTAINTY_MEASURE_WITH_UNIT (LENGTH_MEASURE( 1.000000000000000082E-05 ), #17400, 'distance_accuracy_value', 'NONE');
#4948=ADVANCED_FACE ( 'NONE', ( #16780, #8150 ), #7960, .T. ) ;
#4975=ORIENTED_EDGE ( 'NONE', *, *, #15493, .T. ) ;
#4987=ORIENTED_EDGE ( 'NONE', *, *, #6720, .T. ) ;
#5004=VECTOR ( 'NONE', #91, 1000.000000000000114 ) ;
#5005=ORIENTED_EDGE ( 'NONE', *, *, #6984, .T. ) ;
#5027=FACE_OUTER_BOUND ( 'NONE', #4489, .T. ) ;
#5046=DIRECTION ( 'NONE',  ( 1.000000000000000000, 0.000000000000000000, 0.000000000000000000 ) ) ;
#5048=CARTESIAN_POINT ( 'NONE',  ( 2.500000000000000000, 1.178949249685212974, -2.042000000000001148 ) ) ;
#5059=PLANE ( 'NONE',  #18864 ) ;
#5130=ORIENTED_EDGE ( 'NONE', *, *, #15022, .T. ) ;
#5137=DIRECTION ( 'NONE',  ( 0.000000000000000000, -1.224646799147353454E-16, 1.000000000000000000 ) ) ;
#5144=CARTESIAN_POINT ( 'NONE',  ( 2.500000000000000000, 2.357898499370431722, -2.818925648462311528E-15 ) ) ;
#5162=DIRECTION ( 'NONE',  ( 1.000000000000000000, 0.000000000000000000, 0.000000000000000000 ) ) ;
#5205=ORIENTED_EDGE ( 'NONE', *, *, #9486, .F. ) ;
#5211=AXIS2_PLACEMENT_3D ( 'NONE', #2044, #1955, #10862 ) ;
#5215=DIRECTION ( 'NONE',  ( 0.000000000000000000, 0.000000000000000000, 1.000000000000000000 ) ) ;
#5232=ORIENTED_EDGE ( 'NONE', *, *, #17550, .F. ) ;
#5271=CARTESIAN_POINT ( 'NONE',  ( 2.500000000000000000, -1.178949249685214307, 2.042000000000002036 ) ) ;
#5290=EDGE_LOOP ( 'NONE', ( #8510, #18971 ) ) ;
#5349=VECTOR ( 'NONE', #12818, 1000.000000000000114 ) ;
#5483=DIRECTION ( 'NONE',  ( -1.000000000000000000, -0.000000000000000000, -0.000000000000000000 ) ) ;
#5524=ORIENTED_EDGE ( 'NONE', *, *, #2433, .F. ) ;
#5533=AXIS2_PLACEMENT_3D ( 'NONE', #18062, #10589, #18263 ) ;
#5539=LINE ( 'NONE', #17486, #14273 ) ;
#5543=( NAMED_UNIT ( * ) SI_UNIT ( $, .STERADIAN. ) SOLID_ANGLE_UNIT ( ) );
#5554=FACE_OUTER_BOUND ( 'NONE', #14896, .T. ) ;
#5581=DIRECTION ( 'NONE',  ( -1.000000000000000000, -0.000000000000000000, -0.000000000000000000 ) ) ;
#5639=AXIS2_PLACEMENT_3D ( 'NONE', #939, #1037, #9939 ) ;
#5650=DIRECTION ( 'NONE',  ( 0.000000000000000000, 0.000000000000000000, -1.000000000000000000 ) ) ;
#5651=CIRCLE ( 'NONE', #9402, 2.500000000000000444 ) ;
#5658=ORIENTED_EDGE ( 'NONE', *, *, #3795, .F. ) ;
#5670=VERTEX_POINT ( 'NONE', #11706 ) ;
#5683=PLANE ( 'NONE',  #18798 ) ;
#5727=DIRECTION ( 'NONE',  ( 0.000000000000000000, 0.000000000000000000, 1.000000000000000000 ) ) ;
#5761=CARTESIAN_POINT ( 'NONE',  ( 0.000000000000000000, 5.051668046482832750E-16, -4.000000000000000000 ) ) ;
#5765=EDGE_CURVE ( 'NONE', #111, #13544, #712, .T. ) ;
#5770=CARTESIAN_POINT ( 'NONE',  ( 12.99999999999999822, 0.000000000000000000, 0.000000000000000000 ) ) ;
#5775=DIRECTION ( 'NONE',  ( 0.000000000000000000, 0.000000000000000000, 1.000000000000000000 ) ) ;
#5778=EDGE_LOOP ( 'NONE', ( #1076, #16702, #4893, #5232 ) ) ;
#5810=CIRCLE ( 'NONE', #16782, 2.700000000000000622 ) ;
#5845=DIRECTION ( 'NONE',  ( -1.000000000000000000, -0.000000000000000000, -0.000000000000000000 ) ) ;
#5896=CARTESIAN_POINT ( 'NONE',  ( -31.74999999999995737, 3.061616997868383634E-16, -2.500000000000000444 ) ) ;
#5938=DIRECTION ( 'NONE',  ( 1.000000000000000000, 0.000000000000000000, 0.000000000000000000 ) ) ;
#5951=ORIENTED_EDGE ( 'NONE', *, *, #9014, .F. ) ;
#5978=DIRECTION ( 'NONE',  ( 0.000000000000000000, 0.8660254037844380415, -0.5000000000000011102 ) ) ;
#6032=ORIENTED_EDGE ( 'NONE', *, *, #15148, .F. ) ;
#6066=EDGE_CURVE ( 'NONE', #15191, #10270, #15648, .T. ) ;
#6107=PRODUCT_DEFINITION_CONTEXT ( 'detailed design', #2068, 'design' ) ;
#6112=DIRECTION ( 'NONE',  ( -1.000000000000000000, -0.000000000000000000, -0.000000000000000000 ) ) ;
#6204=DIRECTION ( 'NONE',  ( 0.000000000000000000, 0.000000000000000000, 1.000000000000000000 ) ) ;
#6225=EDGE_LOOP ( 'NONE', ( #13723, #3360, #8887, #2920, #5951, #17856 ) ) ;
#6281=ADVANCED_FACE ( 'NONE', ( #7585 ), #16203, .F. ) ;
#6315=FACE_OUTER_BOUND ( 'NONE', #5778, .T. ) ;
#6348=CARTESIAN_POINT ( 'NONE',  ( 12.99999999999999822, 0.000000000000000000, 0.000000000000000000 ) ) ;
#6410=EDGE_LOOP ( 'NONE', ( #3333, #8231, #9292, #954 ) ) ;
#6418=ADVANCED_FACE ( 'NONE', ( #9243 ), #1871, .F. ) ;
#6423=EDGE_LOOP ( 'NONE', ( #15863, #4103, #19166, #15389 ) ) ;
#6443=EDGE_LOOP ( 'NONE', ( #7055, #10895, #11146, #17516 ) ) ;
#6466=FACE_OUTER_BOUND ( 'NONE', #6423, .T. ) ;
#6496=DIRECTION ( 'NONE',  ( 0.000000000000000000, -1.287488025362403787E-15, -1.000000000000000000 ) ) ;
#6506=PRESENTATION_STYLE_ASSIGNMENT (( #329 ) ) ;
#6517=FACE_OUTER_BOUND ( 'NONE', #14290, .T. ) ;
#6533=SHAPE_REPRESENTATION ( 'socket head cap screw_iso_ISO 4762 M5 x 8 - 8N', ( #1791 ), #9226 ) ;
#6597=LINE ( 'NONE', #18564, #10841 ) ;
#6605=CARTESIAN_POINT ( 'NONE',  ( -31.74999999999995737, 0.000000000000000000, 4.250000000000000000 ) ) ;
#6613=VECTOR ( 'NONE', #13931, 1000.000000000000000 ) ;
#6617=CARTESIAN_POINT ( 'NONE',  ( 5.199999999999996625, 0.000000000000000000, 0.000000000000000000 ) ) ;
#6684=LINE ( 'NONE', #14026, #6613 ) ;
#6699=DIRECTION ( 'NONE',  ( 0.000000000000000000, -0.5000000000000013323, -0.8660254037844380415 ) ) ;
#6720=EDGE_CURVE ( 'NONE', #3232, #13613, #10189, .T. ) ;
#6788=FACE_OUTER_BOUND ( 'NONE', #14972, .T. ) ;
#6880=TOROIDAL_SURFACE ( 'NONE', #19096, 4.000000000000000000, 0.2500000000000000000 ) ;
#6897=CARTESIAN_POINT ( 'NONE',  ( 2.500000000000000000, 0.000000000000000000, 0.000000000000000000 ) ) ;
#6956=VERTEX_POINT ( 'NONE', #10687 ) ;
#6981=DIRECTION ( 'NONE',  ( 0.000000000000000000, 0.000000000000000000, -1.000000000000000000 ) ) ;
#6984=EDGE_CURVE ( 'NONE', #13613, #3035, #5651, .T. ) ;
#6989=DIRECTION ( 'NONE',  ( -1.000000000000000000, -0.000000000000000000, -0.000000000000000000 ) ) ;
#7020=LINE ( 'NONE', #5271, #9115 ) ;
#7037=LINE ( 'NONE', #4502, #15694 ) ;
#7055=ORIENTED_EDGE ( 'NONE', *, *, #6720, .F. ) ;
#7100=DIRECTION ( 'NONE',  ( 0.000000000000000000, 0.000000000000000000, 1.000000000000000000 ) ) ;
#7130=LINE ( 'NONE', #18906, #2249 ) ;
#7180=DIRECTION ( 'NONE',  ( 0.000000000000000000, 0.000000000000000000, 1.000000000000000000 ) ) ;
#7185=AXIS2_PLACEMENT_3D ( 'NONE', #4652, #8747, #10805 ) ;
#7192=LINE ( 'NONE', #12779, #9523 ) ;
#7199=SURFACE_SIDE_STYLE ('',( #19265 ) ) ;
#7218=EDGE_CURVE ( 'NONE', #8108, #13491, #10340, .T. ) ;
#7225=AXIS2_PLACEMENT_3D ( 'NONE', #1382, #10582, #8920 ) ;
#7256=ORIENTED_EDGE ( 'NONE', *, *, #11176, .T. ) ;
#7272=SHAPE_DEFINITION_REPRESENTATION ( #1289, #6533 ) ;
#7278=ORIENTED_EDGE ( 'NONE', *, *, #10580, .T. ) ;
#7311=CARTESIAN_POINT ( 'NONE',  ( 2.500000000000000000, 2.357898499370431722, -2.818925648462311528E-15 ) ) ;
#7326=DIRECTION ( 'NONE',  ( -1.000000000000000000, -0.000000000000000000, -0.000000000000000000 ) ) ;
#7358=EDGE_LOOP ( 'NONE', ( #18640, #16800, #4191, #17423 ) ) ;
#7377=AXIS2_PLACEMENT_3D ( 'NONE', #8614, #12830, #1166 ) ;
#7397=ORIENTED_EDGE ( 'NONE', *, *, #9739, .F. ) ;
#7412=CARTESIAN_POINT ( 'NONE',  ( 12.55500000000001748, 0.000000000000000000, 2.500000000000000444 ) ) ;
#7420=CARTESIAN_POINT ( 'NONE',  ( 5.199999999999996625, 0.000000000000000000, 0.000000000000000000 ) ) ;
#7430=DIRECTION ( 'NONE',  ( -1.000000000000000000, -0.000000000000000000, -0.000000000000000000 ) ) ;
#7439=DIRECTION ( 'NONE',  ( 0.000000000000000000, 0.000000000000000000, -1.000000000000000000 ) ) ;
#7442=ORIENTED_EDGE ( 'NONE', *, *, #1738, .F. ) ;
#7520=DIRECTION ( 'NONE',  ( 0.000000000000000000, 0.000000000000000000, -1.000000000000000000 ) ) ;
#7535=LINE ( 'NONE', #16661, #5004 ) ;
#7540=DIRECTION ( 'NONE',  ( -1.000000000000000000, -0.000000000000000000, -0.000000000000000000 ) ) ;
#7577=AXIS2_PLACEMENT_3D ( 'NONE', #19332, #219, #6204 ) ;
#7580=AXIS2_PLACEMENT_3D ( 'NONE', #5770, #1262, #15253 ) ;
#7585=FACE_OUTER_BOUND ( 'NONE', #18512, .T. ) ;
#7616=DIRECTION ( 'NONE',  ( -1.000000000000000000, -0.000000000000000000, -0.000000000000000000 ) ) ;
#7646=DIRECTION ( 'NONE',  ( 1.000000000000000000, 0.000000000000000000, 0.000000000000000000 ) ) ;
#7648=VERTEX_POINT ( 'NONE', #2653 ) ;
#7677=PRODUCT_DEFINITION_FORMATION_WITH_SPECIFIED_SOURCE ( 'ANY', '', #1449, .NOT_KNOWN. ) ;
#7702=DIRECTION ( 'NONE',  ( 0.000000000000000000, 0.000000000000000000, -1.000000000000000000 ) ) ;
#7707=VECTOR ( 'NONE', #14264, 999.9999999999997726 ) ;
#7758=LINE ( 'NONE', #14015, #2225 ) ;
#7782=ORIENTED_EDGE ( 'NONE', *, *, #17380, .F. ) ;
#7789=FACE_OUTER_BOUND ( 'NONE', #5290, .T. ) ;
#7862=CARTESIAN_POINT ( 'NONE',  ( 4.999999999999997335, 3.306546357697854226E-16, 2.700000000000000622 ) ) ;
#7874=CARTESIAN_POINT ( 'NONE',  ( 2.500000000000000000, 1.178949249685212974, -2.042000000000001148 ) ) ;
#7895=FACE_BOUND ( 'NONE', #8405, .T. ) ;
#7960=PLANE ( 'NONE',  #14720 ) ;
#7968=FACE_OUTER_BOUND ( 'NONE', #426, .T. ) ;
#8014=EDGE_LOOP ( 'NONE', ( #14327, #401, #14938, #5524 ) ) ;
#8041=ORIENTED_EDGE ( 'NONE', *, *, #4222, .F. ) ;
#8078=DIRECTION ( 'NONE',  ( -0.000000000000000000, 1.000000000000000000, 1.224646799147353207E-16 ) ) ;
#8100=ADVANCED_FACE ( 'NONE', ( #5554 ), #17504, .F. ) ;
#8108=VERTEX_POINT ( 'NONE', #11510 ) ;
#8118=ORIENTED_EDGE ( 'NONE', *, *, #18199, .F. ) ;
#8133=AXIS2_PLACEMENT_3D ( 'NONE', #14397, #5483, #13212 ) ;
#8150=FACE_OUTER_BOUND ( 'NONE', #9426, .T. ) ;
#8165=AXIS2_PLACEMENT_3D ( 'NONE', #4707, #9003, #16366 ) ;
#8231=ORIENTED_EDGE ( 'NONE', *, *, #6066, .F. ) ;
#8244=ORIENTED_EDGE ( 'NONE', *, *, #9739, .T. ) ;
#8252=CARTESIAN_POINT ( 'NONE',  ( 2.500000000000000000, -1.178949249685214307, 2.042000000000002036 ) ) ;
#8327=CARTESIAN_POINT ( 'NONE',  ( 2.500000000000000000, 1.178949249685212974, -2.042000000000001148 ) ) ;
#8382=CARTESIAN_POINT ( 'NONE',  ( 0.2500000000000002220, 0.000000000000000000, 4.250000000000000000 ) ) ;
#8393=DIRECTION ( 'NONE',  ( -1.000000000000000000, -0.000000000000000000, -0.000000000000000000 ) ) ;
#8405=EDGE_LOOP ( 'NONE', ( #17338, #15835 ) ) ;
#8437=CARTESIAN_POINT ( 'NONE',  ( 2.500000000000000000, -1.178949249685218970, -2.041999999999998039 ) ) ;
#8489=DIRECTION ( 'NONE',  ( 0.000000000000000000, 1.000000000000000000, -1.471414886128461669E-15 ) ) ;
#8506=VECTOR ( 'NONE', #15960, 1000.000000000000000 ) ;
#8510=ORIENTED_EDGE ( 'NONE', *, *, #4900, .F. ) ;
#8530=ORIENTED_EDGE ( 'NONE', *, *, #10533, .F. ) ;
#8572=( NAMED_UNIT ( * ) PLANE_ANGLE_UNIT ( ) SI_UNIT ( $, .RADIAN. ) );
#8581=LINE ( 'NONE', #14657, #13826 ) ;
#8584=LINE ( 'NONE', #1137, #16228 ) ;
#8606=PLANE ( 'NONE',  #15973 ) ;
#8612=DIRECTION ( 'NONE',  ( 0.000000000000000000, 0.000000000000000000, -1.000000000000000000 ) ) ;
#8614=CARTESIAN_POINT ( 'NONE',  ( 12.99999999999999822, 0.000000000000000000, 0.000000000000000000 ) ) ;
#8695=CARTESIAN_POINT ( 'NONE',  ( 12.55500000000001748, 3.061616997868383634E-16, -2.500000000000000444 ) ) ;
#8699=ORIENTED_EDGE ( 'NONE', *, *, #3546, .T. ) ;
#8743=FACE_OUTER_BOUND ( 'NONE', #7358, .T. ) ;
#8747=DIRECTION ( 'NONE',  ( 1.000000000000000000, 0.000000000000000000, 0.000000000000000000 ) ) ;
#8763=SURFACE_STYLE_USAGE ( .BOTH. , #7199 ) ;
#8798=LINE ( 'NONE', #3904, #8506 ) ;
#8810=ADVANCED_FACE ( 'NONE', ( #17962 ), #1391, .T. ) ;
#8818=ORIENTED_EDGE ( 'NONE', *, *, #2099, .T. ) ;
#8829=DIRECTION ( 'NONE',  ( 0.000000000000000000, -0.5000000000000011102, -0.8660254037844379305 ) ) ;
#8875=FACE_OUTER_BOUND ( 'NONE', #15949, .T. ) ;
#8887=ORIENTED_EDGE ( 'NONE', *, *, #4222, .T. ) ;
#8920=DIRECTION ( 'NONE',  ( 0.000000000000000000, 0.000000000000000000, 1.000000000000000000 ) ) ;
#8923=CARTESIAN_POINT ( 'NONE',  ( 0.000000000000000000, -2.357898499370432610, 3.252606517456513302E-15 ) ) ;
#9003=DIRECTION ( 'NONE',  ( -1.000000000000000000, -0.000000000000000000, -0.000000000000000000 ) ) ;
#9014=EDGE_CURVE ( 'NONE', #3722, #13544, #6684, .T. ) ;
#9074=DIRECTION ( 'NONE',  ( 0.000000000000000000, 0.000000000000000000, 1.000000000000000000 ) ) ;
#9115=VECTOR ( 'NONE', #12899, 1000.000000000000000 ) ;
#9120=ADVANCED_FACE ( 'NONE', ( #702 ), #18510, .F. ) ;
#9130=AXIS2_PLACEMENT_3D ( 'NONE', #9673, #18795, #5650 ) ;
#9151=DIRECTION ( 'NONE',  ( 0.000000000000000000, 0.000000000000000000, 1.000000000000000000 ) ) ;
#9153=ADVANCED_FACE ( 'NONE', ( #9887 ), #19207, .T. ) ;
#9168=ADVANCED_FACE ( 'NONE', ( #2627 ), #5683, .T. ) ;
#9219=ORIENTED_EDGE ( 'NONE', *, *, #7218, .T. ) ;
#9226=( GEOMETRIC_REPRESENTATION_CONTEXT ( 3 ) GLOBAL_UNCERTAINTY_ASSIGNED_CONTEXT ( ( #4939 ) ) GLOBAL_UNIT_ASSIGNED_CONTEXT ( ( #17400, #14179, #5543 ) ) REPRESENTATION_CONTEXT ( 'NONE', 'WORKASPACE' ) );
#9229=PLANE ( 'NONE',  #9863 ) ;
#9243=FACE_OUTER_BOUND ( 'NONE', #16761, .T. ) ;
#9245=EDGE_CURVE ( 'NONE', #11147, #15003, #10331, .T. ) ;
#9289=EDGE_CURVE ( 'NONE', #3232, #9967, #12839, .T. ) ;
#9292=ORIENTED_EDGE ( 'NONE', *, *, #18034, .T. ) ;
#9321=CARTESIAN_POINT ( 'NONE',  ( 0.000000000000000000, 2.357898499370431722, -2.818925648462311528E-15 ) ) ;
#9331=ORIENTED_EDGE ( 'NONE', *, *, #5765, .F. ) ;
#9402=AXIS2_PLACEMENT_3D ( 'NONE', #7420, #14873, #7520 ) ;
#9411=CARTESIAN_POINT ( 'NONE',  ( 0.2500000000000002220, 5.204748896376250699E-16, -4.250000000000000000 ) ) ;
#9420=CIRCLE ( 'NONE', #7225, 2.055000000000000160 ) ;
#9426=EDGE_LOOP ( 'NONE', ( #13104, #12821 ) ) ;
#9441=DIRECTION ( 'NONE',  ( -1.000000000000000000, -0.000000000000000000, -0.000000000000000000 ) ) ;
#9486=EDGE_CURVE ( 'NONE', #513, #4615, #16611, .T. ) ;
#9523=VECTOR ( 'NONE', #18777, 1000.000000000000114 ) ;
#9539=FACE_OUTER_BOUND ( 'NONE', #8014, .T. ) ;
#9555=DIRECTION ( 'NONE',  ( 0.000000000000000000, 0.000000000000000000, -1.000000000000000000 ) ) ;
#9558=AXIS2_PLACEMENT_3D ( 'NONE', #6348, #7616, #16734 ) ;
#9568=CONICAL_SURFACE ( 'NONE', #7377, 2.055000000000000160, 0.7853981633974712606 ) ;
#9581=DIRECTION ( 'NONE',  ( 0.000000000000000000, -1.000000000000000000, 0.000000000000000000 ) ) ;
#9623=( NAMED_UNIT ( * ) PLANE_ANGLE_UNIT ( ) SI_UNIT ( $, .RADIAN. ) );
#9673=CARTESIAN_POINT ( 'NONE',  ( 2.500000000000000000, 2.357898499370431722, -2.818925648462311528E-15 ) ) ;
#9715=AXIS2_PLACEMENT_3D ( 'NONE', #877, #11449, #5775 ) ;
#9718=EDGE_LOOP ( 'NONE', ( #4591, #1071, #8818, #9219, #15872 ) ) ;
#9739=EDGE_CURVE ( 'NONE', #16140, #17064, #7020, .T. ) ;
#9767=LINE ( 'NONE', #13802, #18775 ) ;
#9771=ORIENTED_EDGE ( 'NONE', *, *, #16728, .F. ) ;
#9795=DIRECTION ( 'NONE',  ( 1.000000000000000000, 0.000000000000000000, 0.000000000000000000 ) ) ;
#9801=CARTESIAN_POINT ( 'NONE',  ( 0.000000000000000000, 0.000000000000000000, 0.000000000000000000 ) ) ;
#9823=EDGE_CURVE ( 'NONE', #3035, #12614, #14739, .T. ) ;
#9863=AXIS2_PLACEMENT_3D ( 'NONE', #12365, #1984, #13935 ) ;
#9876=DIRECTION ( 'NONE',  ( 0.000000000000000000, -0.5000000000000011102, -0.8660254037844379305 ) ) ;
#9880=CARTESIAN_POINT ( 'NONE',  ( 2.500000000000000000, 0.000000000000000000, 0.000000000000000000 ) ) ;
#9883=VECTOR ( 'NONE', #14774, 1000.000000000000000 ) ;
#9887=FACE_OUTER_BOUND ( 'NONE', #11517, .T. ) ;
#9939=DIRECTION ( 'NONE',  ( 0.000000000000000000, -1.000000000000000000, 1.471414886128461471E-15 ) ) ;
#9943=CIRCLE ( 'NONE', #1522, 0.2000000000000000944 ) ;
#9962=LINE ( 'NONE', #15965, #5349 ) ;
#9967=VERTEX_POINT ( 'NONE', #7412 ) ;
#9974=DIRECTION ( 'NONE',  ( -1.000000000000000000, -0.000000000000000000, -0.000000000000000000 ) ) ;
#10046=CARTESIAN_POINT ( 'NONE',  ( 2.500000000000000000, 0.000000000000000000, 0.000000000000000000 ) ) ;
#10163=AXIS2_PLACEMENT_3D ( 'NONE', #19309, #5978, #4212 ) ;
#10170=ADVANCED_FACE ( 'NONE', ( #7895, #7789 ), #18386, .T. ) ;
#10172=ADVANCED_FACE ( 'NONE', ( #12478 ), #10612, .F. ) ;
#10189=LINE ( 'NONE', #5896, #14734 ) ;
#10192=PRODUCT_CONTEXT ( 'NONE', #3690, 'mechanical' ) ;
#10210=CARTESIAN_POINT ( 'NONE',  ( 0.000000000000000000, -2.357898499370432610, 3.252606517456513302E-15 ) ) ;
#10214=DIRECTION ( 'NONE',  ( -1.000000000000000000, -0.000000000000000000, -0.000000000000000000 ) ) ;
#10239=CARTESIAN_POINT ( 'NONE',  ( 2.500000000000000000, -2.629050547790028551E-15, -2.041999999999999815 ) ) ;
#10270=VERTEX_POINT ( 'NONE', #9411 ) ;
#10302=DIRECTION ( 'NONE',  ( 0.000000000000000000, 0.000000000000000000, 1.000000000000000000 ) ) ;
#10331=CIRCLE ( 'NONE', #9715, 4.000000000000000000 ) ;
#10340=CIRCLE ( 'NONE', #11584, 2.041999999999999815 ) ;
#10366=ORIENTED_EDGE ( 'NONE', *, *, #9289, .F. ) ;
#10374=ORIENTED_EDGE ( 'NONE', *, *, #4080, .F. ) ;
#10406=ORIENTED_EDGE ( 'NONE', *, *, #377, .T. ) ;
#10413=DIRECTION ( 'NONE',  ( -1.000000000000000000, -0.000000000000000000, -0.000000000000000000 ) ) ;
#10442=CARTESIAN_POINT ( 'NONE',  ( 2.500000000000000000, -2.357898499370432610, 3.252606517456513302E-15 ) ) ;
#10443=ORIENTED_EDGE ( 'NONE', *, *, #18958, .T. ) ;
#10473=( GEOMETRIC_REPRESENTATION_CONTEXT ( 3 ) GLOBAL_UNCERTAINTY_ASSIGNED_CONTEXT ( ( #12170 ) ) GLOBAL_UNIT_ASSIGNED_CONTEXT ( ( #14950, #8572, #11798 ) ) REPRESENTATION_CONTEXT ( 'NONE', 'WORKASPACE' ) );
#10514=CIRCLE ( 'NONE', #11756, 2.500000000000000444 ) ;
#10533=EDGE_CURVE ( 'NONE', #13491, #513, #984, .T. ) ;
#10580=EDGE_CURVE ( 'NONE', #7648, #12574, #18851, .T. ) ;
#10582=DIRECTION ( 'NONE',  ( -1.000000000000000000, -0.000000000000000000, -0.000000000000000000 ) ) ;
#10589=DIRECTION ( 'NONE',  ( 1.000000000000000000, 0.000000000000000000, 0.000000000000000000 ) ) ;
#10612=PLANE ( 'NONE',  #4438 ) ;
#10649=AXIS2_PLACEMENT_3D ( 'NONE', #2870, #6112, #16299 ) ;
#10687=CARTESIAN_POINT ( 'NONE',  ( 2.500000000000000000, 1.178949249685217193, 2.041999999999998483 ) ) ;
#10707=DIRECTION ( 'NONE',  ( -0.5000000000000051070, 1.060575238724903217E-16, -0.8660254037844355990 ) ) ;
#10738=FACE_OUTER_BOUND ( 'NONE', #1985, .T. ) ;
#10800=SURFACE_SIDE_STYLE ('',( #15608 ) ) ;
#10805=DIRECTION ( 'NONE',  ( 0.000000000000000000, 0.000000000000000000, -1.000000000000000000 ) ) ;
#10810=DIRECTION ( 'NONE',  ( 0.000000000000000000, 0.000000000000000000, -1.000000000000000000 ) ) ;
#10841=VECTOR ( 'NONE', #14135, 1000.000000000000000 ) ;
#10842=AXIS2_PLACEMENT_3D ( 'NONE', #2660, #11572, #6981 ) ;
#10862=DIRECTION ( 'NONE',  ( 0.000000000000000000, 0.000000000000000000, 1.000000000000000000 ) ) ;
#10895=ORIENTED_EDGE ( 'NONE', *, *, #9289, .T. ) ;
#10930=LINE ( 'NONE', #4877, #2667 ) ;
#10934=EDGE_CURVE ( 'NONE', #16545, #3619, #17594, .T. ) ;
#10962=VECTOR ( 'NONE', #10707, 1000.000000000000114 ) ;
#10973=EDGE_LOOP ( 'NONE', ( #2514, #7278, #14695, #10366 ) ) ;
#11008=DIRECTION ( 'NONE',  ( 0.000000000000000000, 0.000000000000000000, -1.000000000000000000 ) ) ;
#11104=LINE ( 'NONE', #5048, #14574 ) ;
#11125=DIRECTION ( 'NONE',  ( 0.000000000000000000, 0.000000000000000000, 1.000000000000000000 ) ) ;
#11146=ORIENTED_EDGE ( 'NONE', *, *, #1964, .T. ) ;
#11147=VERTEX_POINT ( 'NONE', #5761 ) ;
#11176=EDGE_CURVE ( 'NONE', #4727, #5670, #7130, .T. ) ;
#11236=CIRCLE ( 'NONE', #8133, 2.041999999999999815 ) ;
#11261=MECHANICAL_DESIGN_GEOMETRIC_PRESENTATION_REPRESENTATION('',(#4734),#2830);
#11271=EDGE_CURVE ( 'NONE', #1736, #513, #8798, .T. ) ;
#11332=DIRECTION ( 'NONE',  ( 0.000000000000000000, 1.000000000000000000, -1.224646799147353207E-16 ) ) ;
#11439=DIRECTION ( 'NONE',  ( 0.000000000000000000, -1.000000000000000000, 1.287488025362403787E-15 ) ) ;
#11449=DIRECTION ( 'NONE',  ( -1.000000000000000000, -0.000000000000000000, -0.000000000000000000 ) ) ;
#11466=ORIENTED_EDGE ( 'NONE', *, *, #7218, .F. ) ;
#11510=CARTESIAN_POINT ( 'NONE',  ( 2.500000000000000000, 1.768423874527823791, 1.020999999999998575 ) ) ;
#11517=EDGE_LOOP ( 'NONE', ( #15554, #2518, #13031, #18565 ) ) ;
#11562=ADVANCED_FACE ( 'NONE', ( #3673 ), #5059, .T. ) ;
#11572=DIRECTION ( 'NONE',  ( 1.000000000000000000, 0.000000000000000000, 0.000000000000000000 ) ) ;
#11579=VECTOR ( 'NONE', #18663, 1000.000000000000000 ) ;
#11584=AXIS2_PLACEMENT_3D ( 'NONE', #40, #10413, #9151 ) ;
#11630=AXIS2_PLACEMENT_3D ( 'NONE', #11778, #17770, #10302 ) ;
#11646=FACE_OUTER_BOUND ( 'NONE', #14498, .T. ) ;
#11705=CARTESIAN_POINT ( 'NONE',  ( 12.99999999999999822, 2.516649172247811061E-16, -2.055000000000000160 ) ) ;
#11706=CARTESIAN_POINT ( 'NONE',  ( 0.000000000000000000, 2.357898499370431722, -2.818925648462311528E-15 ) ) ;
#11756=AXIS2_PLACEMENT_3D ( 'NONE', #2977, #16213, #7100 ) ;
#11778=CARTESIAN_POINT ( 'NONE',  ( 4.999999999999997335, 0.000000000000000000, 0.000000000000000000 ) ) ;
#11798=( NAMED_UNIT ( * ) SI_UNIT ( $, .STERADIAN. ) SOLID_ANGLE_UNIT ( ) );
#11807=EDGE_CURVE ( 'NONE', #996, #17064, #4060, .T. ) ;
#11885=EDGE_CURVE ( 'NONE', #12460, #13544, #13449, .T. ) ;
#11912=VECTOR ( 'NONE', #11439, 1000.000000000000000 ) ;
#11922=ORIENTED_EDGE ( 'NONE', *, *, #5765, .T. ) ;
#11943=CARTESIAN_POINT ( 'NONE',  ( 2.500000000000000000, 1.178949249685212974, -2.042000000000001148 ) ) ;
#11996=ADVANCED_FACE ( 'NONE', ( #6315 ), #15027, .F. ) ;
#12073=AXIS2_PLACEMENT_3D ( 'NONE', #5144, #14965, #18482 ) ;
#12078=ORIENTED_EDGE ( 'NONE', *, *, #18199, .T. ) ;
#12102=LINE ( 'NONE', #19274, #18455 ) ;
#12107=LINE ( 'NONE', #7311, #1778 ) ;
#12131=EDGE_CURVE ( 'NONE', #10270, #11147, #13759, .T. ) ;
#12170=UNCERTAINTY_MEASURE_WITH_UNIT (LENGTH_MEASURE( 1.000000000000000082E-05 ), #14950, 'distance_accuracy_value', 'NONE');
#12191=ORIENTED_EDGE ( 'NONE', *, *, #18958, .F. ) ;
#12260=CARTESIAN_POINT ( 'NONE',  ( 12.99999999999999822, 0.000000000000000000, 2.055000000000000160 ) ) ;
#12296=ORIENTED_EDGE ( 'NONE', *, *, #1457, .F. ) ;
#12365=CARTESIAN_POINT ( 'NONE',  ( 2.500000000000000000, -2.357898499370432610, 3.252606517456513302E-15 ) ) ;
#12410=ORIENTED_EDGE ( 'NONE', *, *, #15493, .F. ) ;
#12460=VERTEX_POINT ( 'NONE', #8923 ) ;
#12478=FACE_OUTER_BOUND ( 'NONE', #242, .T. ) ;
#12504=VERTEX_POINT ( 'NONE', #17756 ) ;
#12542=DIRECTION ( 'NONE',  ( 0.000000000000000000, 0.000000000000000000, 1.000000000000000000 ) ) ;
#12553=CARTESIAN_POINT ( 'NONE',  ( 0.000000000000000000, 0.000000000000000000, 0.000000000000000000 ) ) ;
#12574=VERTEX_POINT ( 'NONE', #12260 ) ;
#12586=UNCERTAINTY_MEASURE_WITH_UNIT (LENGTH_MEASURE( 1.000000000000000082E-05 ), #3654, 'distance_accuracy_value', 'NONE');
#12603=CARTESIAN_POINT ( 'NONE',  ( 0.2500000000000002220, 0.000000000000000000, 0.000000000000000000 ) ) ;
#12614=VERTEX_POINT ( 'NONE', #7862 ) ;
#12645=DIRECTION ( 'NONE',  ( -1.000000000000000000, 0.000000000000000000, -0.000000000000000000 ) ) ;
#12661=LINE ( 'NONE', #6605, #11579 ) ;
#12779=CARTESIAN_POINT ( 'NONE',  ( 12.99999999999999822, 0.000000000000000000, 2.055000000000000160 ) ) ;
#12804=AXIS2_PLACEMENT_3D ( 'NONE', #427, #8078, #5137 ) ;
#12807=ORIENTED_EDGE ( 'NONE', *, *, #641, .F. ) ;
#12818=DIRECTION ( 'NONE',  ( 0.000000000000000000, -0.5000000000000011102, -0.8660254037844379305 ) ) ;
#12821=ORIENTED_EDGE ( 'NONE', *, *, #9245, .T. ) ;
#12829=CARTESIAN_POINT ( 'NONE',  ( 12.55500000000001748, 0.000000000000000000, 0.000000000000000000 ) ) ;
#12830=DIRECTION ( 'NONE',  ( -1.000000000000000000, -0.000000000000000000, -0.000000000000000000 ) ) ;
#12839=CIRCLE ( 'NONE', #1265, 2.500000000000000444 ) ;
#12899=DIRECTION ( 'NONE',  ( 0.000000000000000000, 1.000000000000000000, -1.471414886128461669E-15 ) ) ;
#12924=DIRECTION ( 'NONE',  ( 0.000000000000000000, 0.000000000000000000, 1.000000000000000000 ) ) ;
#12925=FACE_OUTER_BOUND ( 'NONE', #10973, .T. ) ;
#12935=EDGE_CURVE ( 'NONE', #16140, #14750, #19009, .T. ) ;
#12962=ADVANCED_FACE ( 'NONE', ( #1635 ), #8606, .F. ) ;
#12995=ORIENTED_EDGE ( 'NONE', *, *, #3795, .T. ) ;
#13031=ORIENTED_EDGE ( 'NONE', *, *, #15261, .T. ) ;
#13079=AXIS2_PLACEMENT_3D ( 'NONE', #18003, #4578, #9074 ) ;
#13104=ORIENTED_EDGE ( 'NONE', *, *, #19183, .T. ) ;
#13115=CARTESIAN_POINT ( 'NONE',  ( 4.999999999999999112, 0.000000000000000000, 0.000000000000000000 ) ) ;
#13141=CIRCLE ( 'NONE', #3768, 4.250000000000000000 ) ;
#13172=PRESENTATION_STYLE_ASSIGNMENT (( #8763 ) ) ;
#13212=DIRECTION ( 'NONE',  ( 0.000000000000000000, 0.000000000000000000, 1.000000000000000000 ) ) ;
#13424=EDGE_LOOP ( 'NONE', ( #17421, #17351, #5205 ) ) ;
#13449=LINE ( 'NONE', #10210, #1563 ) ;
#13465=CIRCLE ( 'NONE', #10649, 2.700000000000000622 ) ;
#13478=CARTESIAN_POINT ( 'NONE',  ( 2.500000000000000000, 2.357898499370431722, -2.818925648462311528E-15 ) ) ;
#13491=VERTEX_POINT ( 'NONE', #2388 ) ;
#13495=ORIENTED_EDGE ( 'NONE', *, *, #16313, .T. ) ;
#13544=VERTEX_POINT ( 'NONE', #4355 ) ;
#13613=VERTEX_POINT ( 'NONE', #15035 ) ;
#13713=CARTESIAN_POINT ( 'NONE',  ( 0.000000000000000000, 0.000000000000000000, 0.000000000000000000 ) ) ;
#13723=ORIENTED_EDGE ( 'NONE', *, *, #1738, .T. ) ;
#13726=EDGE_CURVE ( 'NONE', #4727, #13491, #3371, .T. ) ;
#13759=CIRCLE ( 'NONE', #12804, 0.2500000000000002220 ) ;
#13790=CARTESIAN_POINT ( 'NONE',  ( 0.000000000000000000, -1.178949249685214307, 2.042000000000002036 ) ) ;
#13802=CARTESIAN_POINT ( 'NONE',  ( -31.74999999999995737, 0.000000000000000000, 2.500000000000000444 ) ) ;
#13826=VECTOR ( 'NONE', #8489, 1000.000000000000000 ) ;
#13841=LINE ( 'NONE', #18457, #4887 ) ;
#13931=DIRECTION ( 'NONE',  ( 0.000000000000000000, -1.000000000000000000, 1.287488025362403787E-15 ) ) ;
#13935=DIRECTION ( 'NONE',  ( 0.000000000000000000, -0.4999999999999991118, 0.8660254037844390407 ) ) ;
#13948=DIRECTION ( 'NONE',  ( 0.000000000000000000, 0.000000000000000000, -1.000000000000000000 ) ) ;
#14015=CARTESIAN_POINT ( 'NONE',  ( 2.500000000000000000, -1.178949249685214307, 2.042000000000002036 ) ) ;
#14026=CARTESIAN_POINT ( 'NONE',  ( 0.000000000000000000, 1.178949249685212974, -2.042000000000001148 ) ) ;
#14035=ORIENTED_EDGE ( 'NONE', *, *, #1964, .F. ) ;
#14045=CIRCLE ( 'NONE', #15294, 2.041999999999999815 ) ;
#14065=VECTOR ( 'NONE', #2451, 1000.000000000000000 ) ;
#14070=CARTESIAN_POINT ( 'NONE',  ( 0.000000000000000000, 1.178949249685217193, 2.041999999999998483 ) ) ;
#14114=CARTESIAN_POINT ( 'NONE',  ( 5.199999999999996625, 0.000000000000000000, 2.500000000000000444 ) ) ;
#14120=DIRECTION ( 'NONE',  ( -1.000000000000000000, -0.000000000000000000, -0.000000000000000000 ) ) ;
#14135=DIRECTION ( 'NONE',  ( 0.000000000000000000, 1.000000000000000000, -1.471414886128461669E-15 ) ) ;
#14140=CARTESIAN_POINT ( 'NONE',  ( -31.74999999999995737, 0.000000000000000000, 0.000000000000000000 ) ) ;
#14148=AXIS2_PLACEMENT_3D ( 'NONE', #3565, #340, #10810 ) ;
#14179=( NAMED_UNIT ( * ) PLANE_ANGLE_UNIT ( ) SI_UNIT ( $, .RADIAN. ) );
#14250=DIRECTION ( 'NONE',  ( -1.000000000000000000, -0.000000000000000000, -0.000000000000000000 ) ) ;
#14258=AXIS2_PLACEMENT_3D ( 'NONE', #7874, #6496, #15420 ) ;
#14264=DIRECTION ( 'NONE',  ( 0.000000000000000000, -0.5000000000000013323, -0.8660254037844380415 ) ) ;
#14273=VECTOR ( 'NONE', #4063, 1000.000000000000114 ) ;
#14290=EDGE_LOOP ( 'NONE', ( #8118, #10374, #12296 ) ) ;
#14327=ORIENTED_EDGE ( 'NONE', *, *, #15896, .F. ) ;
#14397=CARTESIAN_POINT ( 'NONE',  ( 2.500000000000000000, 0.000000000000000000, 0.000000000000000000 ) ) ;
#14404=ORIENTED_EDGE ( 'NONE', *, *, #13726, .F. ) ;
#14440=AXIS2_PLACEMENT_3D ( 'NONE', #9880, #1063, #17255 ) ;
#14457=ORIENTED_EDGE ( 'NONE', *, *, #11807, .T. ) ;
#14466=FACE_OUTER_BOUND ( 'NONE', #16050, .T. ) ;
#14498=EDGE_LOOP ( 'NONE', ( #8041, #18413, #12995, #2851, #14776 ) ) ;
#14504=DIRECTION ( 'NONE',  ( -1.000000000000000000, -0.000000000000000000, -0.000000000000000000 ) ) ;
#14574=VECTOR ( 'NONE', #71, 1000.000000000000000 ) ;
#14657=CARTESIAN_POINT ( 'NONE',  ( 0.000000000000000000, -1.178949249685214307, 2.042000000000002036 ) ) ;
#14695=ORIENTED_EDGE ( 'NONE', *, *, #16728, .T. ) ;
#14720=AXIS2_PLACEMENT_3D ( 'NONE', #12553, #12645, #15593 ) ;
#14732=CYLINDRICAL_SURFACE ( 'NONE', #16616, 4.250000000000000000 ) ;
#14733=ORIENTED_EDGE ( 'NONE', *, *, #3878, .F. ) ;
#14734=VECTOR ( 'NONE', #19228, 1000.000000000000000 ) ;
#14739=CIRCLE ( 'NONE', #17250, 0.2000000000000000944 ) ;
#14750=VERTEX_POINT ( 'NONE', #13790 ) ;
#14774=DIRECTION ( 'NONE',  ( 0.000000000000000000, 0.4999999999999991118, -0.8660254037844391517 ) ) ;
#14776=ORIENTED_EDGE ( 'NONE', *, *, #641, .T. ) ;
#14797=ADVANCED_FACE ( 'NONE', ( #12925 ), #9568, .T. ) ;
#14873=DIRECTION ( 'NONE',  ( 1.000000000000000000, 0.000000000000000000, 0.000000000000000000 ) ) ;
#14874=ORIENTED_EDGE ( 'NONE', *, *, #11885, .F. ) ;
#14888=ORIENTED_EDGE ( 'NONE', *, *, #13726, .T. ) ;
#14896=EDGE_LOOP ( 'NONE', ( #15623, #16777, #8530 ) ) ;
#14909=ADVANCED_FACE ( 'NONE', ( #10738 ), #1101, .T. ) ;
#14938=ORIENTED_EDGE ( 'NONE', *, *, #3447, .F. ) ;
#14950=( LENGTH_UNIT ( ) NAMED_UNIT ( * ) SI_UNIT ( .MILLI., .METRE. ) );
#14965=DIRECTION ( 'NONE',  ( 1.000000000000000000, 0.000000000000000000, 0.000000000000000000 ) ) ;
#14972=EDGE_LOOP ( 'NONE', ( #13495, #4401, #6032, #14404, #7256 ) ) ;
#15003=VERTEX_POINT ( 'NONE', #18407 ) ;
#15022=EDGE_CURVE ( 'NONE', #4615, #111, #10930, .T. ) ;
#15027=TOROIDAL_SURFACE ( 'NONE', #2795, 2.700000000000000622, 0.2000000000000000111 ) ;
#15035=CARTESIAN_POINT ( 'NONE',  ( 5.199999999999996625, 3.061616997868383634E-16, -2.500000000000000444 ) ) ;
#15116=DIRECTION ( 'NONE',  ( 0.000000000000000000, -0.5000000000000013323, -0.8660254037844380415 ) ) ;
#15148=EDGE_CURVE ( 'NONE', #13491, #1736, #2215, .T. ) ;
#15166=PLANE ( 'NONE',  #12073 ) ;
#15181=ORIENTED_EDGE ( 'NONE', *, *, #18393, .T. ) ;
#15191=VERTEX_POINT ( 'NONE', #8382 ) ;
#15226=CIRCLE ( 'NONE', #815, 4.250000000000000000 ) ;
#15248=CARTESIAN_POINT ( 'NONE',  ( 2.500000000000000000, 2.357898499370431722, -2.818925648462311528E-15 ) ) ;
#15253=DIRECTION ( 'NONE',  ( 0.000000000000000000, 0.000000000000000000, 1.000000000000000000 ) ) ;
#15261=EDGE_CURVE ( 'NONE', #10270, #15191, #15226, .T. ) ;
#15294=AXIS2_PLACEMENT_3D ( 'NONE', #10046, #16042, #846 ) ;
#15389=ORIENTED_EDGE ( 'NONE', *, *, #18034, .F. ) ;
#15420=DIRECTION ( 'NONE',  ( 0.000000000000000000, 1.000000000000000000, -1.287488025362403787E-15 ) ) ;
#15426=EDGE_CURVE ( 'NONE', #9967, #3232, #10514, .T. ) ;
#15493=EDGE_CURVE ( 'NONE', #4727, #8108, #5539, .T. ) ;
#15494=EDGE_LOOP ( 'NONE', ( #5658, #8244, #18925 ) ) ;
#15521=DIRECTION ( 'NONE',  ( 1.000000000000000000, 0.000000000000000000, 0.000000000000000000 ) ) ;
#15554=ORIENTED_EDGE ( 'NONE', *, *, #4900, .T. ) ;
#15593=DIRECTION ( 'NONE',  ( -0.000000000000000000, 0.000000000000000000, 1.000000000000000000 ) ) ;
#15597=DIRECTION ( 'NONE',  ( -1.000000000000000000, -0.000000000000000000, -0.000000000000000000 ) ) ;
#15608=SURFACE_STYLE_FILL_AREA ( #610 ) ;
#15623=ORIENTED_EDGE ( 'NONE', *, *, #15148, .T. ) ;
#15648=CIRCLE ( 'NONE', #18167, 4.250000000000000000 ) ;
#15694=VECTOR ( 'NONE', #7430, 1000.000000000000000 ) ;
#15757=PLANE ( 'NONE',  #5639 ) ;
#15778=LINE ( 'NONE', #8327, #11912 ) ;
#15788=DIRECTION ( 'NONE',  ( 0.000000000000000000, 0.000000000000000000, 1.000000000000000000 ) ) ;
#15795=DIRECTION ( 'NONE',  ( 0.000000000000000000, 0.000000000000000000, 1.000000000000000000 ) ) ;
#15835=ORIENTED_EDGE ( 'NONE', *, *, #17550, .T. ) ;
#15853=CARTESIAN_POINT ( 'NONE',  ( 5.199999999999996625, 3.306546357697854226E-16, 2.700000000000000622 ) ) ;
#15863=ORIENTED_EDGE ( 'NONE', *, *, #15261, .F. ) ;
#15872=ORIENTED_EDGE ( 'NONE', *, *, #10533, .T. ) ;
#15896=EDGE_CURVE ( 'NONE', #3035, #13613, #828, .T. ) ;
#15949=EDGE_LOOP ( 'NONE', ( #4910, #4987, #5005, #14035 ) ) ;
#15960=DIRECTION ( 'NONE',  ( 0.000000000000000000, -1.000000000000000000, 1.287488025362403787E-15 ) ) ;
#15965=CARTESIAN_POINT ( 'NONE',  ( 0.000000000000000000, -1.178949249685214307, 2.042000000000002036 ) ) ;
#15973=AXIS2_PLACEMENT_3D ( 'NONE', #13478, #5938, #7702 ) ;
#16042=DIRECTION ( 'NONE',  ( -1.000000000000000000, -0.000000000000000000, -0.000000000000000000 ) ) ;
#16050=EDGE_LOOP ( 'NONE', ( #10406, #3119, #12191, #7397, #17159 ) ) ;
#16069=PLANE ( 'NONE',  #10163 ) ;
#16140=VERTEX_POINT ( 'NONE', #8252 ) ;
#16203=PLANE ( 'NONE',  #7185 ) ;
#16213=DIRECTION ( 'NONE',  ( -1.000000000000000000, -0.000000000000000000, -0.000000000000000000 ) ) ;
#16228=VECTOR ( 'NONE', #8393, 1000.000000000000000 ) ;
#16266=ORIENTED_EDGE ( 'NONE', *, *, #16407, .T. ) ;
#16296=ADVANCED_FACE ( 'NONE', ( #1885 ), #411, .F. ) ;
#16299=DIRECTION ( 'NONE',  ( 0.000000000000000000, 0.000000000000000000, -1.000000000000000000 ) ) ;
#16313=EDGE_CURVE ( 'NONE', #5670, #3722, #3356, .T. ) ;
#16337=DIRECTION ( 'NONE',  ( 0.000000000000000000, -0.4999999999999993894, 0.8660254037844389297 ) ) ;
#16356=VERTEX_POINT ( 'NONE', #18160 ) ;
#16366=DIRECTION ( 'NONE',  ( 0.000000000000000000, 0.000000000000000000, 1.000000000000000000 ) ) ;
#16407=EDGE_CURVE ( 'NONE', #8108, #6956, #12107, .T. ) ;
#16477=CARTESIAN_POINT ( 'NONE',  ( 2.500000000000000000, -1.178949249685214307, 2.042000000000002036 ) ) ;
#16479=ADVANCED_BREP_SHAPE_REPRESENTATION ( '', ( #3611, #1791 ), #9226 ) ;
#16496=VECTOR ( 'NONE', #15116, 999.9999999999997726 ) ;
#16545=VERTEX_POINT ( 'NONE', #2213 ) ;
#16606=CARTESIAN_POINT ( 'NONE',  ( 2.500000000000000000, 0.000000000000000000, 0.000000000000000000 ) ) ;
#16611=CIRCLE ( 'NONE', #8165, 2.041999999999999815 ) ;
#16616=AXIS2_PLACEMENT_3D ( 'NONE', #14140, #18375, #16797 ) ;
#16629=LINE ( 'NONE', #11705, #19373 ) ;
#16648=ORIENTED_EDGE ( 'NONE', *, *, #10580, .F. ) ;
#16661=CARTESIAN_POINT ( 'NONE',  ( 0.000000000000000000, 2.357898499370431722, -2.818925648462311528E-15 ) ) ;
#16673=ORIENTED_EDGE ( 'NONE', *, *, #632, .T. ) ;
#16702=ORIENTED_EDGE ( 'NONE', *, *, #6984, .F. ) ;
#16728=EDGE_CURVE ( 'NONE', #12574, #9967, #7192, .T. ) ;
#16734=DIRECTION ( 'NONE',  ( 0.000000000000000000, 0.000000000000000000, 1.000000000000000000 ) ) ;
#16736=ORIENTED_EDGE ( 'NONE', *, *, #11271, .F. ) ;
#16761=EDGE_LOOP ( 'NONE', ( #7782, #8699, #19100, #2347, #14457 ) ) ;
#16777=ORIENTED_EDGE ( 'NONE', *, *, #11271, .T. ) ;
#16780=FACE_BOUND ( 'NONE', #6225, .T. ) ;
#16782=AXIS2_PLACEMENT_3D ( 'NONE', #13115, #7540, #7439 ) ;
#16797=DIRECTION ( 'NONE',  ( 0.000000000000000000, 0.000000000000000000, 1.000000000000000000 ) ) ;
#16800=ORIENTED_EDGE ( 'NONE', *, *, #10934, .T. ) ;
#16932=DIRECTION ( 'NONE',  ( 0.000000000000000000, 0.4999999999999991118, -0.8660254037844391517 ) ) ;
#16945=VECTOR ( 'NONE', #8829, 1000.000000000000114 ) ;
#16971=CARTESIAN_POINT ( 'NONE',  ( 0.2500000000000002220, 0.000000000000000000, 0.000000000000000000 ) ) ;
#17064=VERTEX_POINT ( 'NONE', #721 ) ;
#17088=( NAMED_UNIT ( * ) SI_UNIT ( $, .STERADIAN. ) SOLID_ANGLE_UNIT ( ) );
#17092=EDGE_LOOP ( 'NONE', ( #7442, #17757, #4975, #16266, #18348 ) ) ;
#17159=ORIENTED_EDGE ( 'NONE', *, *, #12935, .T. ) ;
#17181=DIRECTION ( 'NONE',  ( 0.000000000000000000, 0.5000000000000011102, 0.8660254037844379305 ) ) ;
#17250=AXIS2_PLACEMENT_3D ( 'NONE', #15853, #11332, #17324 ) ;
#17255=DIRECTION ( 'NONE',  ( 0.000000000000000000, 0.000000000000000000, 1.000000000000000000 ) ) ;
#17266=VERTEX_POINT ( 'NONE', #1889 ) ;
#17295=ADVANCED_FACE ( 'NONE', ( #7968 ), #9229, .T. ) ;
#17324=DIRECTION ( 'NONE',  ( 0.000000000000000000, 1.224646799147353207E-16, 1.000000000000000000 ) ) ;
#17338=ORIENTED_EDGE ( 'NONE', *, *, #3447, .T. ) ;
#17351=ORIENTED_EDGE ( 'NONE', *, *, #15022, .F. ) ;
#17379=ADVANCED_FACE ( 'NONE', ( #5027 ), #3359, .F. ) ;
#17380=EDGE_CURVE ( 'NONE', #17266, #17064, #13841, .T. ) ;
#17400=( LENGTH_UNIT ( ) NAMED_UNIT ( * ) SI_UNIT ( .MILLI., .METRE. ) );
#17421=ORIENTED_EDGE ( 'NONE', *, *, #4208, .T. ) ;
#17423=ORIENTED_EDGE ( 'NONE', *, *, #6066, .T. ) ;
#17478=CARTESIAN_POINT ( 'NONE',  ( 2.500000000000000000, -1.768423874527823569, 1.021000000000002794 ) ) ;
#17486=CARTESIAN_POINT ( 'NONE',  ( 2.500000000000000000, 2.357898499370431722, -2.818925648462311528E-15 ) ) ;
#17504=PLANE ( 'NONE',  #9130 ) ;
#17516=ORIENTED_EDGE ( 'NONE', *, *, #15896, .T. ) ;
#17539=COLOUR_RGB ( '', 0.09019608, 0.27058824, 0.51372549) ;
#17550=EDGE_CURVE ( 'NONE', #12614, #16356, #5810, .T. ) ;
#17594=CIRCLE ( 'NONE', #11630, 4.250000000000000000 ) ;
#17647=ADVANCED_FACE ( 'NONE', ( #11646 ), #16069, .T. ) ;
#17699=DIRECTION ( 'NONE',  ( -0.7071067811865312525, 8.659560562355131306E-17, -0.7071067811865637820 ) ) ;
#17756=CARTESIAN_POINT ( 'NONE',  ( 2.500000000000000000, -2.357898499370432610, 3.252606517456513302E-15 ) ) ;
#17757=ORIENTED_EDGE ( 'NONE', *, *, #11176, .F. ) ;
#17770=DIRECTION ( 'NONE',  ( -1.000000000000000000, -0.000000000000000000, -0.000000000000000000 ) ) ;
#17787=ADVANCED_FACE ( 'NONE', ( #6466 ), #1745, .T. ) ;
#17792=SHAPE_REPRESENTATION_RELATIONSHIP ( 'NONE' , 'NONE' ,  #6533, #16479 ) ;
#17856=ORIENTED_EDGE ( 'NONE', *, *, #16313, .F. ) ;
#17932=CLOSED_SHELL ( 'NONE', ( #6418, #17787, #18371, #14909, #2309, #9153, #4948, #3556, #10170, #8810, #14797, #9168, #11996, #3260, #11562, #4602, #17647, #17295, #17379, #3701, #16296, #18367, #12962, #10172, #6281, #8100, #9120 ) ) ;
#17962=FACE_OUTER_BOUND ( 'NONE', #6443, .T. ) ;
#18003=CARTESIAN_POINT ( 'NONE',  ( -31.74999999999995737, 0.000000000000000000, 0.000000000000000000 ) ) ;
#18034=EDGE_CURVE ( 'NONE', #15191, #15003, #3947, .T. ) ;
#18062=CARTESIAN_POINT ( 'NONE',  ( 2.500000000000000000, 2.357898499370431722, -2.818925648462311528E-15 ) ) ;
#18072=PRODUCT_DEFINITION ( 'UNKNOWN', '', #7677, #6107 ) ;
#18160=CARTESIAN_POINT ( 'NONE',  ( 4.999999999999997335, 0.000000000000000000, -2.700000000000000622 ) ) ;
#18167=AXIS2_PLACEMENT_3D ( 'NONE', #16971, #18543, #12542 ) ;
#18175=LINE ( 'NONE', #4753, #10962 ) ;
#18189=AXIS2_PLACEMENT_3D ( 'NONE', #2555, #892, #17181 ) ;
#18199=EDGE_CURVE ( 'NONE', #12504, #4615, #2709, .T. ) ;
#18263=DIRECTION ( 'NONE',  ( 0.000000000000000000, 0.000000000000000000, -1.000000000000000000 ) ) ;
#18304=CARTESIAN_POINT ( 'NONE',  ( 5.199999999999996625, 0.000000000000000000, -2.700000000000000622 ) ) ;
#18348=ORIENTED_EDGE ( 'NONE', *, *, #4240, .T. ) ;
#18367=ADVANCED_FACE ( 'NONE', ( #6517 ), #15166, .F. ) ;
#18371=ADVANCED_FACE ( 'NONE', ( #9539 ), #1443, .F. ) ;
#18375=DIRECTION ( 'NONE',  ( -1.000000000000000000, -0.000000000000000000, -0.000000000000000000 ) ) ;
#18386=PLANE ( 'NONE',  #14148 ) ;
#18393=EDGE_CURVE ( 'NONE', #1736, #3722, #11104, .T. ) ;
#18407=CARTESIAN_POINT ( 'NONE',  ( 0.000000000000000000, 0.000000000000000000, 4.000000000000000000 ) ) ;
#18413=ORIENTED_EDGE ( 'NONE', *, *, #12935, .F. ) ;
#18455=VECTOR ( 'NONE', #5845, 1000.000000000000000 ) ;
#18457=CARTESIAN_POINT ( 'NONE',  ( 2.500000000000000000, 0.000000000000000000, 2.041999999999999815 ) ) ;
#18478=CARTESIAN_POINT ( 'NONE',  ( 2.500000000000000000, 2.357898499370431722, -2.818925648462311528E-15 ) ) ;
#18482=DIRECTION ( 'NONE',  ( 0.000000000000000000, 0.000000000000000000, -1.000000000000000000 ) ) ;
#18510=CONICAL_SURFACE ( 'NONE', #2206, 2.041999999999999815, 1.047197551196591858 ) ;
#18512=EDGE_LOOP ( 'NONE', ( #12410, #14888, #11466 ) ) ;
#18543=DIRECTION ( 'NONE',  ( 1.000000000000000000, 0.000000000000000000, 0.000000000000000000 ) ) ;
#18564=CARTESIAN_POINT ( 'NONE',  ( 2.500000000000000000, -1.178949249685214307, 2.042000000000002036 ) ) ;
#18565=ORIENTED_EDGE ( 'NONE', *, *, #3664, .F. ) ;
#18572=ORIENTED_EDGE ( 'NONE', *, *, #15426, .F. ) ;
#18579=DIRECTION ( 'NONE',  ( 0.000000000000000000, 0.000000000000000000, -1.000000000000000000 ) ) ;
#18640=ORIENTED_EDGE ( 'NONE', *, *, #2101, .F. ) ;
#18663=DIRECTION ( 'NONE',  ( -1.000000000000000000, -0.000000000000000000, -0.000000000000000000 ) ) ;
#18682=DIRECTION ( 'NONE',  ( 0.000000000000000000, -0.8660254037844390407, -0.4999999999999994449 ) ) ;
#18691=DIRECTION ( 'NONE',  ( 0.000000000000000000, -1.000000000000000000, 0.000000000000000000 ) ) ;
#18775=VECTOR ( 'NONE', #383, 1000.000000000000000 ) ;
#18777=DIRECTION ( 'NONE',  ( -0.7071067811865312525, 0.000000000000000000, 0.7071067811865637820 ) ) ;
#18795=DIRECTION ( 'NONE',  ( 1.000000000000000000, 0.000000000000000000, 0.000000000000000000 ) ) ;
#18798=AXIS2_PLACEMENT_3D ( 'NONE', #2441, #9795, #8612 ) ;
#18851=CIRCLE ( 'NONE', #7580, 2.055000000000000160 ) ;
#18864=AXIS2_PLACEMENT_3D ( 'NONE', #15248, #18682, #1818 ) ;
#18906=CARTESIAN_POINT ( 'NONE',  ( 2.500000000000000000, 2.357898499370431722, -2.818925648462311528E-15 ) ) ;
#18912=CARTESIAN_POINT ( 'NONE',  ( 2.500000000000000000, -1.178949249685214307, 2.042000000000002036 ) ) ;
#18925=ORIENTED_EDGE ( 'NONE', *, *, #11807, .F. ) ;
#18958=EDGE_CURVE ( 'NONE', #17064, #6956, #6597, .T. ) ;
#18971=ORIENTED_EDGE ( 'NONE', *, *, #10934, .F. ) ;
#19008=ORIENTED_EDGE ( 'NONE', *, *, #16407, .F. ) ;
#19009=LINE ( 'NONE', #18912, #3125 ) ;
#19053=CARTESIAN_POINT ( 'NONE',  ( 4.999999999999997335, 0.000000000000000000, 0.000000000000000000 ) ) ;
#19074=AXIS2_PLACEMENT_3D ( 'NONE', #6897, #14250, #820 ) ;
#19096=AXIS2_PLACEMENT_3D ( 'NONE', #19152, #6989, #7180 ) ;
#19100=ORIENTED_EDGE ( 'NONE', *, *, #9486, .T. ) ;
#19152=CARTESIAN_POINT ( 'NONE',  ( 0.2500000000000002220, 0.000000000000000000, 0.000000000000000000 ) ) ;
#19166=ORIENTED_EDGE ( 'NONE', *, *, #19183, .F. ) ;
#19183=EDGE_CURVE ( 'NONE', #15003, #11147, #1480, .T. ) ;
#19207=CYLINDRICAL_SURFACE ( 'NONE', #3472, 4.250000000000000000 ) ;
#19224=LINE ( 'NONE', #16477, #16945 ) ;
#19228=DIRECTION ( 'NONE',  ( -1.000000000000000000, -0.000000000000000000, -0.000000000000000000 ) ) ;
#19265=SURFACE_STYLE_FILL_AREA ( #2591 ) ;
#19274=CARTESIAN_POINT ( 'NONE',  ( 2.500000000000000000, -2.357898499370432610, 3.252606517456513302E-15 ) ) ;
#19285=AXIS2_PLACEMENT_3D ( 'NONE', #3612, #9581, #2238 ) ;
#19309=CARTESIAN_POINT ( 'NONE',  ( 2.500000000000000000, -1.178949249685214307, 2.042000000000002036 ) ) ;
#19332=CARTESIAN_POINT ( 'NONE',  ( -31.74999999999995737, 0.000000000000000000, 0.000000000000000000 ) ) ;
#19373=VECTOR ( 'NONE', #17699, 1000.000000000000114 ) ;
ENDSEC;
END-ISO-10303-21;
